ISO-10303-21;
HEADER;
FILE_DESCRIPTION (('STEP AP203'),
    '1' );
FILE_NAME ('bench vise5-.step',
    '2026-10-07T23:37:23',
    ( '' ),
    ( '' ),
    'SwSTEP 2.0',
    'SolidWorks 2024',
    '' );
FILE_SCHEMA (( 'AUTOMOTIVE_DESIGN' ));
ENDSEC;

DATA;
#3=CARTESIAN_POINT ( 'NONE',  ( 2.750000000000000444, 8.719000000000002970, 4.313750000000002416 ) ) ;
#31=EDGE_LOOP ( 'NONE', ( #4317, #4718, #4653 ) ) ;
#40=DIRECTION ( 'NONE',  ( -1.000000000000000000, 0.000000000000000000, 0.000000000000000000 ) ) ;
#58=CARTESIAN_POINT ( 'NONE',  ( -2.740000000000001545, 7.973999999999999311, 4.323750000000001315 ) ) ;
#75=VECTOR ( 'NONE', #6916, 39.37007874015748854 ) ;
#79=EDGE_CURVE ( 'NONE', #5487, #520, #4524, .T. ) ;
#93=DIRECTION ( 'NONE',  ( 0.7071067811865474617, -0.7071067811865474617, -0.000000000000000000 ) ) ;
#101=EDGE_LOOP ( 'NONE', ( #3409, #718, #7066 ) ) ;
#115=DIRECTION ( 'NONE',  ( 0.000000000000000000, -1.000000000000000000, -0.000000000000000000 ) ) ;
#128=ORIENTED_EDGE ( 'NONE', *, *, #4388, .F. ) ;
#146=EDGE_LOOP ( 'NONE', ( #7906, #6476, #5872, #8033 ) ) ;
#155=LINE ( 'NONE', #7705, #5155 ) ;
#169=CARTESIAN_POINT ( 'NONE',  ( 2.740000000000001545, 8.729000000000002757, 3.833750000000001545 ) ) ;
#183=CARTESIAN_POINT ( 'NONE',  ( -2.750000000000000444, 8.719000000000002970, 3.833750000000001545 ) ) ;
#192=EDGE_LOOP ( 'NONE', ( #5190, #7911, #4806, #6907 ) ) ;
#202=LINE ( 'NONE', #3233, #5994 ) ;
#212=VERTEX_POINT ( 'NONE', #6416 ) ;
#219=EDGE_LOOP ( 'NONE', ( #243, #2322, #241, #301 ) ) ;
#221=AXIS2_PLACEMENT_3D ( 'NONE', #6097, #3140, #4902 ) ;
#237=EDGE_CURVE ( 'NONE', #1328, #4455, #5336, .T. ) ;
#241=ORIENTED_EDGE ( 'NONE', *, *, #381, .T. ) ;
#243=ORIENTED_EDGE ( 'NONE', *, *, #1327, .T. ) ;
#248=ORIENTED_EDGE ( 'NONE', *, *, #2346, .T. ) ;
#285=CARTESIAN_POINT ( 'NONE',  ( 2.740000000000001545, 8.729000000000002757, 3.833750000000001545 ) ) ;
#296=EDGE_CURVE ( 'NONE', #3365, #941, #4687, .T. ) ;
#301=ORIENTED_EDGE ( 'NONE', *, *, #296, .T. ) ;
#327=ADVANCED_FACE ( 'NONE', ( #1012 ), #2235, .T. ) ;
#336=CARTESIAN_POINT ( 'NONE',  ( -2.740000000000001545, 8.729000000000002757, 3.823750000000002647 ) ) ;
#345=ADVANCED_FACE ( 'NONE', ( #2970 ), #1788, .F. ) ;
#354=AXIS2_PLACEMENT_3D ( 'NONE', #6437, #7092, #3840 ) ;
#373=PLANE ( 'NONE',  #3594 ) ;
#381=EDGE_CURVE ( 'NONE', #3887, #3365, #3166, .T. ) ;
#390=ORIENTED_EDGE ( 'NONE', *, *, #1733, .T. ) ;
#411=ADVANCED_FACE ( 'NONE', ( #2487 ), #596, .F. ) ;
#446=PLANE ( 'NONE',  #5451 ) ;
#472=CARTESIAN_POINT ( 'NONE',  ( 2.740000000000001545, 8.729000000000002757, 3.833750000000001545 ) ) ;
#499=EDGE_LOOP ( 'NONE', ( #1524, #3936, #1377, #8105 ) ) ;
#500=DIRECTION ( 'NONE',  ( 1.000000000000000000, 0.000000000000000000, 0.000000000000000000 ) ) ;
#501=EDGE_CURVE ( 'NONE', #5362, #7817, #3859, .T. ) ;
#511=CARTESIAN_POINT ( 'NONE',  ( -2.750000000000000444, 7.973999999999999311, 3.823750000000002647 ) ) ;
#512=ORIENTED_EDGE ( 'NONE', *, *, #2568, .F. ) ;
#520=VERTEX_POINT ( 'NONE', #169 ) ;
#528=ORIENTED_EDGE ( 'NONE', *, *, #4439, .F. ) ;
#541=CARTESIAN_POINT ( 'NONE',  ( 2.740000000000001545, 7.973999999999999311, 3.823750000000002647 ) ) ;
#550=ORIENTED_EDGE ( 'NONE', *, *, #7199, .F. ) ;
#574=VECTOR ( 'NONE', #2841, 39.37007874015748143 ) ;
#577=ORIENTED_EDGE ( 'NONE', *, *, #5901, .F. ) ;
#578=SHAPE_REPRESENTATION ( 'bench vise5-', ( #7272 ), #5419 ) ;
#579=VECTOR ( 'NONE', #785, 39.37007874015748143 ) ;
#580=AXIS2_PLACEMENT_3D ( 'NONE', #2554, #7584, #115 ) ;
#581=CARTESIAN_POINT ( 'NONE',  ( -2.750000000000000444, 8.729000000000002757, 3.823750000000002647 ) ) ;
#596=PLANE ( 'NONE',  #1000 ) ;
#635=DIRECTION ( 'NONE',  ( 0.000000000000000000, 1.000000000000000000, 0.000000000000000000 ) ) ;
#669=DIRECTION ( 'NONE',  ( 1.000000000000000000, 0.000000000000000000, -0.000000000000000000 ) ) ;
#684=CARTESIAN_POINT ( 'NONE',  ( 2.740000000000001545, 7.964000000000000412, 4.313750000000002416 ) ) ;
#686=ADVANCED_FACE ( 'NONE', ( #1004 ), #2801, .T. ) ;
#689=CARTESIAN_POINT ( 'NONE',  ( -2.750000000000000444, 7.973999999999999311, 3.823750000000002647 ) ) ;
#697=DIRECTION ( 'NONE',  ( 1.000000000000000000, 0.000000000000000000, 0.000000000000000000 ) ) ;
#703=FACE_OUTER_BOUND ( 'NONE', #499, .T. ) ;
#704=DIRECTION ( 'NONE',  ( -0.7071067811865474617, 0.000000000000000000, 0.7071067811865474617 ) ) ;
#706=ORIENTED_EDGE ( 'NONE', *, *, #79, .T. ) ;
#718=ORIENTED_EDGE ( 'NONE', *, *, #4210, .T. ) ;
#731=EDGE_CURVE ( 'NONE', #4455, #1007, #1052, .T. ) ;
#742=VECTOR ( 'NONE', #5859, 39.37007874015748143 ) ;
#747=VECTOR ( 'NONE', #7304, 39.37007874015748854 ) ;
#769=PRODUCT_DEFINITION_SHAPE ( 'NONE', 'NONE',  #3521 ) ;
#774=EDGE_LOOP ( 'NONE', ( #7821, #2662, #6671 ) ) ;
#785=DIRECTION ( 'NONE',  ( 0.000000000000000000, 0.000000000000000000, -1.000000000000000000 ) ) ;
#795=EDGE_LOOP ( 'NONE', ( #4269, #4259, #5089, #128 ) ) ;
#803=CARTESIAN_POINT ( 'NONE',  ( -2.750000000000000444, 7.964000000000000412, 3.833750000000001545 ) ) ;
#810=FACE_OUTER_BOUND ( 'NONE', #795, .T. ) ;
#816=ORIENTED_EDGE ( 'NONE', *, *, #4210, .F. ) ;
#831=DIRECTION ( 'NONE',  ( 0.7071067811865474617, 0.7071067811865474617, -0.000000000000000000 ) ) ;
#865=FACE_OUTER_BOUND ( 'NONE', #192, .T. ) ;
#870=ORIENTED_EDGE ( 'NONE', *, *, #6187, .F. ) ;
#914=CARTESIAN_POINT ( 'NONE',  ( -2.740000000000001545, 8.729000000000002757, 4.313750000000002416 ) ) ;
#941=VERTEX_POINT ( 'NONE', #6099 ) ;
#955=UNCERTAINTY_MEASURE_WITH_UNIT (LENGTH_MEASURE( 1.000000000000000082E-05 ), #2427, 'distance_accuracy_value', 'NONE');
#991=EDGE_LOOP ( 'NONE', ( #6821, #1517, #4310 ) ) ;
#995=DIRECTION ( 'NONE',  ( -0.000000000000000000, -0.7071067811865475727, -0.7071067811865475727 ) ) ;
#998=ORIENTED_EDGE ( 'NONE', *, *, #2689, .T. ) ;
#1000=AXIS2_PLACEMENT_3D ( 'NONE', #4934, #4894, #669 ) ;
#1004=FACE_OUTER_BOUND ( 'NONE', #7933, .T. ) ;
#1007=VERTEX_POINT ( 'NONE', #6792 ) ;
#1009=CARTESIAN_POINT ( 'NONE',  ( 2.750000000000000444, 8.719000000000002970, 3.823750000000002647 ) ) ;
#1012=FACE_OUTER_BOUND ( 'NONE', #1498, .T. ) ;
#1052=LINE ( 'NONE', #1009, #5446 ) ;
#1056=FACE_OUTER_BOUND ( 'NONE', #4658, .T. ) ;
#1093=VECTOR ( 'NONE', #2380, 39.37007874015748854 ) ;
#1118=CARTESIAN_POINT ( 'NONE',  ( 0.000000000000000000, 7.973999999999999311, 4.323750000000001315 ) ) ;
#1130=DIRECTION ( 'NONE',  ( -0.7071067811865474617, 0.000000000000000000, -0.7071067811865474617 ) ) ;
#1142=ORIENTED_EDGE ( 'NONE', *, *, #7781, .T. ) ;
#1171=MECHANICAL_CONTEXT ( 'NONE', #5651, 'mechanical' ) ;
#1181=DIRECTION ( 'NONE',  ( 0.5773502691896257311, -0.5773502691896257311, 0.5773502691896257311 ) ) ;
#1196=LINE ( 'NONE', #2959, #2680 ) ;
#1206=DIRECTION ( 'NONE',  ( 0.7071067811865474617, -0.000000000000000000, 0.7071067811865474617 ) ) ;
#1231=PLANE ( 'NONE',  #6654 ) ;
#1233=VECTOR ( 'NONE', #5399, 39.37007874015748854 ) ;
#1244=DIRECTION ( 'NONE',  ( -0.7071067811865474617, -0.000000000000000000, -0.7071067811865474617 ) ) ;
#1260=AXIS2_PLACEMENT_3D ( 'NONE', #6807, #3076, #1314 ) ;
#1301=DIRECTION ( 'NONE',  ( 0.7071067811865474617, 0.000000000000000000, -0.7071067811865474617 ) ) ;
#1311=CARTESIAN_POINT ( 'NONE',  ( 2.740000000000001545, 7.964000000000000412, 4.313750000000002416 ) ) ;
#1314=DIRECTION ( 'NONE',  ( -1.000000000000000000, 0.000000000000000000, 0.000000000000000000 ) ) ;
#1322=EDGE_CURVE ( 'NONE', #2476, #4355, #6729, .T. ) ;
#1327=EDGE_CURVE ( 'NONE', #941, #5487, #6624, .T. ) ;
#1328=VERTEX_POINT ( 'NONE', #2837 ) ;
#1339=CARTESIAN_POINT ( 'NONE',  ( -2.740000000000001545, 0.000000000000000000, 4.323750000000001315 ) ) ;
#1353=CARTESIAN_POINT ( 'NONE',  ( 2.740000000000001545, 7.964000000000000412, 4.313750000000002416 ) ) ;
#1354=VECTOR ( 'NONE', #1898, 39.37007874015748854 ) ;
#1355=VECTOR ( 'NONE', #5681, 39.37007874015748143 ) ;
#1362=DIRECTION ( 'NONE',  ( 1.000000000000000000, 0.000000000000000000, 0.000000000000000000 ) ) ;
#1377=ORIENTED_EDGE ( 'NONE', *, *, #7885, .F. ) ;
#1378=VECTOR ( 'NONE', #7948, 39.37007874015748854 ) ;
#1384=ORIENTED_EDGE ( 'NONE', *, *, #8012, .F. ) ;
#1425=FACE_OUTER_BOUND ( 'NONE', #3014, .T. ) ;
#1445=CARTESIAN_POINT ( 'NONE',  ( 2.750000000000000444, 7.973999999999999311, 4.313750000000002416 ) ) ;
#1447=ADVANCED_FACE ( 'NONE', ( #6930 ), #1929, .F. ) ;
#1456=VERTEX_POINT ( 'NONE', #5038 ) ;
#1479=EDGE_CURVE ( 'NONE', #5688, #5130, #3157, .T. ) ;
#1497=CARTESIAN_POINT ( 'NONE',  ( -2.750000000000000444, 8.719000000000002970, 3.833750000000001545 ) ) ;
#1498=EDGE_LOOP ( 'NONE', ( #3162, #4098, #6279, #5676 ) ) ;
#1502=ADVANCED_FACE ( 'NONE', ( #6315 ), #1231, .T. ) ;
#1517=ORIENTED_EDGE ( 'NONE', *, *, #7885, .T. ) ;
#1520=DIRECTION ( 'NONE',  ( 0.5773502691896257311, 0.5773502691896257311, -0.5773502691896257311 ) ) ;
#1524=ORIENTED_EDGE ( 'NONE', *, *, #6938, .T. ) ;
#1532=APPLICATION_CONTEXT ( 'configuration controlled 3d designs of mechanical parts and assemblies' ) ;
#1581=EDGE_CURVE ( 'NONE', #2711, #4311, #6967, .T. ) ;
#1587=CARTESIAN_POINT ( 'NONE',  ( -2.740000000000001545, 7.964000000000000412, 3.833750000000001545 ) ) ;
#1608=CARTESIAN_POINT ( 'NONE',  ( -2.750000000000000444, 7.964000000000000412, 3.833750000000001545 ) ) ;
#1615=DIRECTION ( 'NONE',  ( 0.7071067811865474617, 0.000000000000000000, 0.7071067811865474617 ) ) ;
#1626=AXIS2_PLACEMENT_3D ( 'NONE', #7841, #4803, #2258 ) ;
#1627=DIRECTION ( 'NONE',  ( 0.000000000000000000, 1.000000000000000000, 0.000000000000000000 ) ) ;
#1674=ADVANCED_FACE ( 'NONE', ( #2052 ), #3916, .T. ) ;
#1683=EDGE_CURVE ( 'NONE', #1007, #4311, #202, .T. ) ;
#1688=( NAMED_UNIT ( * ) SI_UNIT ( $, .STERADIAN. ) SOLID_ANGLE_UNIT ( ) );
#1707=CARTESIAN_POINT ( 'NONE',  ( 2.740000000000001545, 8.719000000000002970, 3.823750000000002647 ) ) ;
#1722=DIRECTION ( 'NONE',  ( -0.7071067811865474617, 0.000000000000000000, 0.7071067811865474617 ) ) ;
#1725=DIRECTION ( 'NONE',  ( 0.000000000000000000, 0.000000000000000000, 1.000000000000000000 ) ) ;
#1733=EDGE_CURVE ( 'NONE', #4311, #1456, #7740, .T. ) ;
#1748=ADVANCED_FACE ( 'NONE', ( #6146 ), #2381, .F. ) ;
#1765=( NAMED_UNIT ( * ) PLANE_ANGLE_UNIT ( ) SI_UNIT ( $, .RADIAN. ) );
#1771=AXIS2_PLACEMENT_3D ( 'NONE', #285, #1520, #4075 ) ;
#1772=MANIFOLD_SOLID_BREP ( 'N', #7427 ) ;
#1778=EDGE_CURVE ( 'NONE', #520, #7817, #8172, .T. ) ;
#1780=AXIS2_PLACEMENT_3D ( 'NONE', #4970, #5661, #635 ) ;
#1788=PLANE ( 'NONE',  #1780 ) ;
#1799=ORIENTED_EDGE ( 'NONE', *, *, #2882, .T. ) ;
#1806=DIRECTION ( 'NONE',  ( -1.000000000000000000, 0.000000000000000000, 0.000000000000000000 ) ) ;
#1845=DIRECTION ( 'NONE',  ( -0.7071067811865474617, -0.7071067811865474617, 0.000000000000000000 ) ) ;
#1872=CARTESIAN_POINT ( 'NONE',  ( -2.740000000000001545, 7.964000000000000412, 3.833750000000001545 ) ) ;
#1876=EDGE_CURVE ( 'NONE', #2620, #6635, #5770, .T. ) ;
#1877=PRODUCT_DEFINITION_FORMATION_WITH_SPECIFIED_SOURCE ( 'ANY', '', #5745, .NOT_KNOWN. ) ;
#1898=DIRECTION ( 'NONE',  ( 0.7071067811865474617, -0.7071067811865474617, -0.000000000000000000 ) ) ;
#1906=CARTESIAN_POINT ( 'NONE',  ( 2.740000000000001545, 8.729000000000002757, 3.833750000000001545 ) ) ;
#1916=VECTOR ( 'NONE', #3169, 39.37007874015748143 ) ;
#1929=PLANE ( 'NONE',  #1260 ) ;
#1932=CARTESIAN_POINT ( 'NONE',  ( 2.750000000000000444, 8.719000000000002970, 3.833750000000001545 ) ) ;
#1934=LINE ( 'NONE', #4426, #2153 ) ;
#1985=ORIENTED_EDGE ( 'NONE', *, *, #7148, .T. ) ;
#2031=LINE ( 'NONE', #3, #5682 ) ;
#2052=FACE_OUTER_BOUND ( 'NONE', #991, .T. ) ;
#2058=DIRECTION ( 'NONE',  ( 0.000000000000000000, 0.000000000000000000, 1.000000000000000000 ) ) ;
#2063=ORIENTED_EDGE ( 'NONE', *, *, #5301, .F. ) ;
#2075=LINE ( 'NONE', #6557, #3725 ) ;
#2120=ORIENTED_EDGE ( 'NONE', *, *, #79, .F. ) ;
#2126=FACE_OUTER_BOUND ( 'NONE', #4568, .T. ) ;
#2129=ADVANCED_FACE ( 'NONE', ( #6790 ), #3051, .T. ) ;
#2135=EDGE_LOOP ( 'NONE', ( #7466, #5348, #870, #4153 ) ) ;
#2142=PLANE ( 'NONE',  #1626 ) ;
#2153=VECTOR ( 'NONE', #2633, 39.37007874015748854 ) ;
#2228=LINE ( 'NONE', #4095, #7395 ) ;
#2235=PLANE ( 'NONE',  #7016 ) ;
#2238=CARTESIAN_POINT ( 'NONE',  ( -2.740000000000001545, 8.729000000000002757, 3.823750000000002647 ) ) ;
#2258=DIRECTION ( 'NONE',  ( 0.000000000000000000, -1.000000000000000000, -0.000000000000000000 ) ) ;
#2276=LINE ( 'NONE', #3547, #747 ) ;
#2287=LINE ( 'NONE', #5390, #1378 ) ;
#2322=ORIENTED_EDGE ( 'NONE', *, *, #6551, .T. ) ;
#2346=EDGE_CURVE ( 'NONE', #5429, #7262, #2869, .T. ) ;
#2369=ORIENTED_EDGE ( 'NONE', *, *, #4131, .T. ) ;
#2380=DIRECTION ( 'NONE',  ( -0.000000000000000000, 0.7071067811865474617, 0.7071067811865474617 ) ) ;
#2381=PLANE ( 'NONE',  #3747 ) ;
#2387=ADVANCED_FACE ( 'NONE', ( #2900 ), #446, .T. ) ;
#2391=DIRECTION ( 'NONE',  ( 0.000000000000000000, 1.000000000000000000, 0.000000000000000000 ) ) ;
#2420=CARTESIAN_POINT ( 'NONE',  ( 0.000000000000000000, 0.000000000000000000, 4.323750000000001315 ) ) ;
#2427=( CONVERSION_BASED_UNIT ( 'INCH', #7958 ) LENGTH_UNIT ( ) NAMED_UNIT ( #7017 ) );
#2437=AXIS2_PLACEMENT_3D ( 'NONE', #3261, #3181, #1301 ) ;
#2441=ADVANCED_FACE ( 'NONE', ( #6304 ), #3718, .T. ) ;
#2443=EDGE_CURVE ( 'NONE', #7113, #2476, #4411, .T. ) ;
#2445=AXIS2_PLACEMENT_3D ( 'NONE', #4679, #7335, #4646 ) ;
#2449=CARTESIAN_POINT ( 'NONE',  ( -2.750000000000000444, 8.719000000000002970, 3.833750000000001545 ) ) ;
#2476=VERTEX_POINT ( 'NONE', #58 ) ;
#2478=CARTESIAN_POINT ( 'NONE',  ( 2.740000000000001545, 8.729000000000002757, 4.313750000000002416 ) ) ;
#2487=FACE_OUTER_BOUND ( 'NONE', #219, .T. ) ;
#2493=EDGE_CURVE ( 'NONE', #5429, #2620, #6798, .T. ) ;
#2551=EDGE_CURVE ( 'NONE', #5362, #2620, #3390, .T. ) ;
#2554=CARTESIAN_POINT ( 'NONE',  ( 2.750000000000000444, 7.964000000000000412, 3.833750000000001545 ) ) ;
#2568=EDGE_CURVE ( 'NONE', #6635, #212, #3302, .T. ) ;
#2620=VERTEX_POINT ( 'NONE', #7814 ) ;
#2633=DIRECTION ( 'NONE',  ( 0.7071067811865474617, 0.7071067811865474617, 0.000000000000000000 ) ) ;
#2656=DIRECTION ( 'NONE',  ( 0.000000000000000000, 1.000000000000000000, 0.000000000000000000 ) ) ;
#2662=ORIENTED_EDGE ( 'NONE', *, *, #5198, .T. ) ;
#2676=ORIENTED_EDGE ( 'NONE', *, *, #5272, .F. ) ;
#2680=VECTOR ( 'NONE', #2391, 39.37007874015748143 ) ;
#2689=EDGE_CURVE ( 'NONE', #5429, #3365, #2276, .T. ) ;
#2691=VECTOR ( 'NONE', #6947, 39.37007874015748854 ) ;
#2697=CARTESIAN_POINT ( 'NONE',  ( -2.745000000000000995, 7.973999999999999311, 3.828750000000002096 ) ) ;
#2711=VERTEX_POINT ( 'NONE', #6708 ) ;
#2714=VECTOR ( 'NONE', #5765, 39.37007874015748143 ) ;
#2742=PLANE ( 'NONE',  #1771 ) ;
#2760=CARTESIAN_POINT ( 'NONE',  ( 2.740000000000001545, 7.964000000000000412, 3.833750000000001545 ) ) ;
#2761=ORIENTED_EDGE ( 'NONE', *, *, #1733, .F. ) ;
#2783=LINE ( 'NONE', #5270, #7537 ) ;
#2801=PLANE ( 'NONE',  #2445 ) ;
#2820=LINE ( 'NONE', #7865, #7116 ) ;
#2829=FACE_OUTER_BOUND ( 'NONE', #6089, .T. ) ;
#2837=CARTESIAN_POINT ( 'NONE',  ( 2.750000000000000444, 7.973999999999999311, 3.833750000000001545 ) ) ;
#2841=DIRECTION ( 'NONE',  ( 0.000000000000000000, 0.000000000000000000, 1.000000000000000000 ) ) ;
#2843=ORIENTED_EDGE ( 'NONE', *, *, #6709, .T. ) ;
#2869=LINE ( 'NONE', #5357, #3628 ) ;
#2882=EDGE_CURVE ( 'NONE', #4311, #520, #5766, .T. ) ;
#2885=DIRECTION ( 'NONE',  ( -0.5773502691896257311, 0.5773502691896257311, 0.5773502691896257311 ) ) ;
#2900=FACE_OUTER_BOUND ( 'NONE', #6016, .T. ) ;
#2904=LINE ( 'NONE', #3492, #1233 ) ;
#2915=ORIENTED_EDGE ( 'NONE', *, *, #1322, .T. ) ;
#2928=EDGE_CURVE ( 'NONE', #1007, #5688, #4910, .T. ) ;
#2954=VERTEX_POINT ( 'NONE', #4533 ) ;
#2959=CARTESIAN_POINT ( 'NONE',  ( 2.740000000000001545, 0.000000000000000000, 4.323750000000001315 ) ) ;
#2963=ORIENTED_EDGE ( 'NONE', *, *, #3739, .F. ) ;
#2968=LINE ( 'NONE', #2449, #7540 ) ;
#2970=FACE_OUTER_BOUND ( 'NONE', #4556, .T. ) ;
#3014=EDGE_LOOP ( 'NONE', ( #5768, #390, #2676 ) ) ;
#3019=DIRECTION ( 'NONE',  ( 0.000000000000000000, -0.000000000000000000, 1.000000000000000000 ) ) ;
#3026=CARTESIAN_POINT ( 'NONE',  ( 2.750000000000000444, 8.729000000000002757, 3.833750000000001545 ) ) ;
#3047=AXIS2_PLACEMENT_3D ( 'NONE', #2420, #3019, #6179 ) ;
#3051=PLANE ( 'NONE',  #221 ) ;
#3065=AXIS2_PLACEMENT_3D ( 'NONE', #5871, #1362, #3849 ) ;
#3072=PLANE ( 'NONE',  #5283 ) ;
#3076=DIRECTION ( 'NONE',  ( 0.000000000000000000, 0.7071067811865475727, -0.7071067811865475727 ) ) ;
#3081=ORIENTED_EDGE ( 'NONE', *, *, #1581, .T. ) ;
#3085=DIRECTION ( 'NONE',  ( 0.000000000000000000, 0.000000000000000000, 1.000000000000000000 ) ) ;
#3109=CARTESIAN_POINT ( 'NONE',  ( 2.740000000000001545, 7.964000000000000412, 3.823750000000002647 ) ) ;
#3114=DIRECTION ( 'NONE',  ( -0.000000000000000000, 0.000000000000000000, 1.000000000000000000 ) ) ;
#3126=DIRECTION ( 'NONE',  ( -1.000000000000000000, 0.000000000000000000, 0.000000000000000000 ) ) ;
#3140=DIRECTION ( 'NONE',  ( -0.5773502691896257311, -0.5773502691896257311, 0.5773502691896257311 ) ) ;
#3149=CARTESIAN_POINT ( 'NONE',  ( 2.750000000000000444, 8.719000000000002970, 3.823750000000002647 ) ) ;
#3156=EDGE_LOOP ( 'NONE', ( #3515, #5568, #5309 ) ) ;
#3157=LINE ( 'NONE', #1353, #4413 ) ;
#3160=PLANE ( 'NONE',  #580 ) ;
#3162=ORIENTED_EDGE ( 'NONE', *, *, #7670, .T. ) ;
#3166=LINE ( 'NONE', #511, #3609 ) ;
#3169=DIRECTION ( 'NONE',  ( -1.000000000000000000, 0.000000000000000000, 0.000000000000000000 ) ) ;
#3181=DIRECTION ( 'NONE',  ( 0.5773502691896257311, 0.5773502691896257311, 0.5773502691896257311 ) ) ;
#3207=VECTOR ( 'NONE', #1627, 39.37007874015748143 ) ;
#3214=AXIS2_PLACEMENT_3D ( 'NONE', #3705, #5466, #7935 ) ;
#3219=VECTOR ( 'NONE', #1806, 39.37007874015748143 ) ;
#3233=CARTESIAN_POINT ( 'NONE',  ( 2.750000000000000444, 8.719000000000002970, 4.313750000000002416 ) ) ;
#3261=CARTESIAN_POINT ( 'NONE',  ( 2.750000000000000444, 8.719000000000002970, 4.313750000000002416 ) ) ;
#3268=EDGE_CURVE ( 'NONE', #7262, #3887, #2783, .T. ) ;
#3293=ORIENTED_EDGE ( 'NONE', *, *, #2689, .F. ) ;
#3301=DIRECTION ( 'NONE',  ( 0.000000000000000000, -1.000000000000000000, 0.000000000000000000 ) ) ;
#3302=LINE ( 'NONE', #3350, #6898 ) ;
#3310=PLANE ( 'NONE',  #7411 ) ;
#3315=EDGE_LOOP ( 'NONE', ( #6185, #4621, #3566, #6069 ) ) ;
#3333=VECTOR ( 'NONE', #5116, 39.37007874015748854 ) ;
#3336=ORIENTED_EDGE ( 'NONE', *, *, #6938, .F. ) ;
#3346=ADVANCED_FACE ( 'N', ( #3405 ), #5517, .T. ) ;
#3350=CARTESIAN_POINT ( 'NONE',  ( -2.750000000000000444, 8.729000000000002757, 4.313750000000002416 ) ) ;
#3355=ORIENTED_EDGE ( 'NONE', *, *, #1778, .F. ) ;
#3364=PLANE ( 'NONE',  #3065 ) ;
#3365=VERTEX_POINT ( 'NONE', #3650 ) ;
#3366=SHAPE_DEFINITION_REPRESENTATION ( #769, #578 ) ;
#3390=LINE ( 'NONE', #803, #2714 ) ;
#3398=CARTESIAN_POINT ( 'NONE',  ( -2.740000000000001545, 7.964000000000000412, 3.823750000000002647 ) ) ;
#3403=ORIENTED_EDGE ( 'NONE', *, *, #2928, .F. ) ;
#3405=FACE_OUTER_BOUND ( 'NONE', #6771, .T. ) ;
#3409=ORIENTED_EDGE ( 'NONE', *, *, #4090, .F. ) ;
#3414=FACE_OUTER_BOUND ( 'NONE', #6483, .T. ) ;
#3431=EDGE_CURVE ( 'NONE', #941, #7817, #4913, .T. ) ;
#3459=AXIS2_PLACEMENT_3D ( 'NONE', #581, #3126, #3085 ) ;
#3491=DIRECTION ( 'NONE',  ( -1.000000000000000000, 0.000000000000000000, 0.000000000000000000 ) ) ;
#3492=CARTESIAN_POINT ( 'NONE',  ( 2.745000000000000995, 7.973999999999999311, 4.318750000000002309 ) ) ;
#3495=ORIENTED_EDGE ( 'NONE', *, *, #5272, .T. ) ;
#3509=DIRECTION ( 'NONE',  ( -0.7071067811865475727, 0.000000000000000000, -0.7071067811865475727 ) ) ;
#3515=ORIENTED_EDGE ( 'NONE', *, *, #5901, .T. ) ;
#3521=PRODUCT_DEFINITION ( 'UNKNOWN', '', #1877, #7625 ) ;
#3534=DIRECTION ( 'NONE',  ( -0.7071067811865475727, 0.7071067811865475727, 0.000000000000000000 ) ) ;
#3541=DIRECTION ( 'NONE',  ( 0.000000000000000000, 0.000000000000000000, 1.000000000000000000 ) ) ;
#3543=CARTESIAN_POINT ( 'NONE',  ( -2.740000000000001545, 8.729000000000002757, 4.313750000000002416 ) ) ;
#3547=CARTESIAN_POINT ( 'NONE',  ( -2.740000000000001545, 7.964000000000000412, 3.833750000000001545 ) ) ;
#3566=ORIENTED_EDGE ( 'NONE', *, *, #2551, .T. ) ;
#3568=DIRECTION ( 'NONE',  ( 1.000000000000000000, 0.000000000000000000, 0.000000000000000000 ) ) ;
#3594=AXIS2_PLACEMENT_3D ( 'NONE', #7185, #6581, #5360 ) ;
#3609=VECTOR ( 'NONE', #40, 39.37007874015748143 ) ;
#3619=VECTOR ( 'NONE', #5883, 39.37007874015748143 ) ;
#3621=LINE ( 'NONE', #7503, #5406 ) ;
#3628=VECTOR ( 'NONE', #7353, 39.37007874015748143 ) ;
#3650=CARTESIAN_POINT ( 'NONE',  ( -2.740000000000001545, 7.973999999999999311, 3.823750000000002647 ) ) ;
#3694=FACE_OUTER_BOUND ( 'NONE', #3315, .T. ) ;
#3705=CARTESIAN_POINT ( 'NONE',  ( -2.750000000000000444, 8.719000000000002970, 3.823750000000002647 ) ) ;
#3718=PLANE ( 'NONE',  #5315 ) ;
#3725=VECTOR ( 'NONE', #7805, 39.37007874015748143 ) ;
#3736=CARTESIAN_POINT ( 'NONE',  ( 0.000000000000000000, 0.000000000000000000, 0.000000000000000000 ) ) ;
#3739=EDGE_CURVE ( 'NONE', #2476, #6635, #7376, .T. ) ;
#3740=EDGE_LOOP ( 'NONE', ( #4543, #2063, #2761, #3782 ) ) ;
#3746=CARTESIAN_POINT ( 'NONE',  ( -2.740000000000001545, 8.719000000000002970, 4.323750000000001315 ) ) ;
#3747=AXIS2_PLACEMENT_3D ( 'NONE', #3149, #6800, #3114 ) ;
#3760=DIRECTION ( 'NONE',  ( 0.7071067811865474617, 0.000000000000000000, -0.7071067811865474617 ) ) ;
#3768=CARTESIAN_POINT ( 'NONE',  ( 2.750000000000000444, 8.729000000000002757, 3.823750000000002647 ) ) ;
#3782=ORIENTED_EDGE ( 'NONE', *, *, #1581, .F. ) ;
#3817=CARTESIAN_POINT ( 'NONE',  ( -2.750000000000000444, 7.964000000000000412, 4.313750000000002416 ) ) ;
#3840=DIRECTION ( 'NONE',  ( -0.7071067811865474617, 0.000000000000000000, -0.7071067811865474617 ) ) ;
#3849=DIRECTION ( 'NONE',  ( 0.000000000000000000, 0.000000000000000000, -1.000000000000000000 ) ) ;
#3859=LINE ( 'NONE', #1497, #6101 ) ;
#3887=VERTEX_POINT ( 'NONE', #541 ) ;
#3916=PLANE ( 'NONE',  #354 ) ;
#3936=ORIENTED_EDGE ( 'NONE', *, *, #237, .F. ) ;
#3983=ADVANCED_FACE ( 'NONE', ( #3414 ), #2142, .F. ) ;
#4025=ADVANCED_FACE ( 'NONE', ( #4638 ), #4092, .F. ) ;
#4054=LINE ( 'NONE', #914, #7954 ) ;
#4075=DIRECTION ( 'NONE',  ( -0.7071067811865474617, 0.000000000000000000, -0.7071067811865474617 ) ) ;
#4078=DIRECTION ( 'NONE',  ( -0.5773502691896257311, -0.5773502691896257311, -0.5773502691896257311 ) ) ;
#4090=EDGE_CURVE ( 'NONE', #2711, #7113, #4054, .T. ) ;
#4092=PLANE ( 'NONE',  #4490 ) ;
#4095=CARTESIAN_POINT ( 'NONE',  ( 2.750000000000000444, 7.973999999999999311, 3.823750000000002647 ) ) ;
#4098=ORIENTED_EDGE ( 'NONE', *, *, #296, .F. ) ;
#4131=EDGE_CURVE ( 'NONE', #7817, #2711, #5953, .T. ) ;
#4138=CARTESIAN_POINT ( 'NONE',  ( 2.750000000000000444, 7.973999999999999311, 3.823750000000002647 ) ) ;
#4153=ORIENTED_EDGE ( 'NONE', *, *, #1322, .F. ) ;
#4169=SHAPE_REPRESENTATION_RELATIONSHIP ( 'NONE' , 'NONE' ,  #578, #7219 ) ;
#4183=EDGE_CURVE ( 'NONE', #212, #5362, #3621, .T. ) ;
#4210=EDGE_CURVE ( 'NONE', #2711, #212, #6812, .T. ) ;
#4259=ORIENTED_EDGE ( 'NONE', *, *, #1876, .F. ) ;
#4266=DIRECTION ( 'NONE',  ( 0.000000000000000000, 0.000000000000000000, -1.000000000000000000 ) ) ;
#4269=ORIENTED_EDGE ( 'NONE', *, *, #5198, .F. ) ;
#4279=DIRECTION ( 'NONE',  ( 0.7071067811865474617, 0.000000000000000000, 0.7071067811865474617 ) ) ;
#4285=ADVANCED_FACE ( 'NONE', ( #3694 ), #7463, .T. ) ;
#4291=LINE ( 'NONE', #3109, #4374 ) ;
#4296=DIRECTION ( 'NONE',  ( -0.000000000000000000, -0.7071067811865474617, 0.7071067811865474617 ) ) ;
#4301=DIRECTION ( 'NONE',  ( 0.000000000000000000, 1.000000000000000000, -0.000000000000000000 ) ) ;
#4310=ORIENTED_EDGE ( 'NONE', *, *, #8176, .F. ) ;
#4311=VERTEX_POINT ( 'NONE', #2478 ) ;
#4317=ORIENTED_EDGE ( 'NONE', *, *, #7670, .F. ) ;
#4355=VERTEX_POINT ( 'NONE', #5121 ) ;
#4367=LINE ( 'NONE', #2697, #6751 ) ;
#4373=CARTESIAN_POINT ( 'NONE',  ( -2.750000000000000444, 8.729000000000002757, 3.833750000000001545 ) ) ;
#4374=VECTOR ( 'NONE', #6796, 39.37007874015748143 ) ;
#4386=DIRECTION ( 'NONE',  ( 0.000000000000000000, 0.7071067811865475727, -0.7071067811865475727 ) ) ;
#4388=EDGE_CURVE ( 'NONE', #2954, #5429, #5700, .T. ) ;
#4390=ORIENTED_EDGE ( 'NONE', *, *, #2443, .F. ) ;
#4411=LINE ( 'NONE', #1339, #5585 ) ;
#4413=VECTOR ( 'NONE', #1845, 39.37007874015748854 ) ;
#4426=CARTESIAN_POINT ( 'NONE',  ( 2.750000000000000444, 7.973999999999999311, 3.833750000000001545 ) ) ;
#4439=EDGE_CURVE ( 'NONE', #7262, #5130, #155, .T. ) ;
#4455=VERTEX_POINT ( 'NONE', #1932 ) ;
#4478=LINE ( 'NONE', #6296, #7000 ) ;
#4479=ORIENTED_EDGE ( 'NONE', *, *, #381, .F. ) ;
#4490=AXIS2_PLACEMENT_3D ( 'NONE', #4138, #3534, #6661 ) ;
#4524=LINE ( 'NONE', #1906, #2691 ) ;
#4531=DIRECTION ( 'NONE',  ( 0.7071067811865474617, 0.000000000000000000, -0.7071067811865474617 ) ) ;
#4533=CARTESIAN_POINT ( 'NONE',  ( -2.740000000000001545, 7.964000000000000412, 4.313750000000002416 ) ) ;
#4543=ORIENTED_EDGE ( 'NONE', *, *, #4090, .T. ) ;
#4556=EDGE_LOOP ( 'NONE', ( #7734, #512, #2963, #4390 ) ) ;
#4568=EDGE_LOOP ( 'NONE', ( #706, #1142, #3336 ) ) ;
#4621=ORIENTED_EDGE ( 'NONE', *, *, #4183, .T. ) ;
#4633=ORIENTED_EDGE ( 'NONE', *, *, #1479, .T. ) ;
#4638=FACE_OUTER_BOUND ( 'NONE', #5758, .T. ) ;
#4646=DIRECTION ( 'NONE',  ( 0.000000000000000000, -0.000000000000000000, -1.000000000000000000 ) ) ;
#4653=ORIENTED_EDGE ( 'NONE', *, *, #3431, .F. ) ;
#4658=EDGE_LOOP ( 'NONE', ( #816, #7742, #6644, #6140 ) ) ;
#4666=DIRECTION ( 'NONE',  ( 0.000000000000000000, 0.7071067811865474617, -0.7071067811865474617 ) ) ;
#4679=CARTESIAN_POINT ( 'NONE',  ( -2.750000000000000444, 7.964000000000000412, 3.823750000000002647 ) ) ;
#4687=LINE ( 'NONE', #2238, #3207 ) ;
#4707=PLANE ( 'NONE',  #6484 ) ;
#4717=CARTESIAN_POINT ( 'NONE',  ( 2.750000000000000444, 7.973999999999999311, 3.833750000000001545 ) ) ;
#4718=ORIENTED_EDGE ( 'NONE', *, *, #501, .T. ) ;
#4721=ADVANCED_FACE ( 'NONE', ( #2829 ), #4707, .T. ) ;
#4745=VECTOR ( 'NONE', #1615, 39.37007874015748854 ) ;
#4748=VECTOR ( 'NONE', #3301, 39.37007874015748143 ) ;
#4803=DIRECTION ( 'NONE',  ( -0.7071067811865475727, 0.000000000000000000, -0.7071067811865475727 ) ) ;
#4806=ORIENTED_EDGE ( 'NONE', *, *, #7199, .T. ) ;
#4816=LINE ( 'NONE', #5423, #5043 ) ;
#4894=DIRECTION ( 'NONE',  ( 0.000000000000000000, -0.000000000000000000, 1.000000000000000000 ) ) ;
#4902=DIRECTION ( 'NONE',  ( 0.7071067811865474617, 0.000000000000000000, 0.7071067811865474617 ) ) ;
#4910=LINE ( 'NONE', #6471, #4748 ) ;
#4913=LINE ( 'NONE', #7321, #1093 ) ;
#4934=CARTESIAN_POINT ( 'NONE',  ( 0.000000000000000000, 0.000000000000000000, 3.823750000000002647 ) ) ;
#4940=ADVANCED_FACE ( 'NONE', ( #810 ), #3310, .F. ) ;
#4970=CARTESIAN_POINT ( 'NONE',  ( -2.750000000000000444, 8.729000000000002757, 4.313750000000002416 ) ) ;
#5012=EDGE_LOOP ( 'NONE', ( #2369, #3081, #1799, #6051 ) ) ;
#5038=CARTESIAN_POINT ( 'NONE',  ( 2.740000000000001545, 8.719000000000002970, 4.323750000000001315 ) ) ;
#5043=VECTOR ( 'NONE', #1206, 39.37007874015748854 ) ;
#5089=ORIENTED_EDGE ( 'NONE', *, *, #2493, .F. ) ;
#5110=ORIENTED_EDGE ( 'NONE', *, *, #8176, .T. ) ;
#5116=DIRECTION ( 'NONE',  ( -0.000000000000000000, -0.7071067811865474617, -0.7071067811865474617 ) ) ;
#5121=CARTESIAN_POINT ( 'NONE',  ( 2.740000000000001545, 7.973999999999999311, 4.323750000000001315 ) ) ;
#5130=VERTEX_POINT ( 'NONE', #8031 ) ;
#5155=VECTOR ( 'NONE', #2058, 39.37007874015748143 ) ;
#5160=CARTESIAN_POINT ( 'NONE',  ( -2.750000000000000444, 8.719000000000002970, 3.833750000000001545 ) ) ;
#5190=ORIENTED_EDGE ( 'NONE', *, *, #731, .T. ) ;
#5193=LINE ( 'NONE', #1311, #3333 ) ;
#5198=EDGE_CURVE ( 'NONE', #6635, #2954, #4478, .T. ) ;
#5270=CARTESIAN_POINT ( 'NONE',  ( 2.740000000000001545, 7.969000000000000306, 3.828750000000002096 ) ) ;
#5272=EDGE_CURVE ( 'NONE', #1007, #1456, #2031, .T. ) ;
#5283=AXIS2_PLACEMENT_3D ( 'NONE', #3768, #4301, #1725 ) ;
#5287=LINE ( 'NONE', #4717, #4745 ) ;
#5301=EDGE_CURVE ( 'NONE', #1456, #7113, #2075, .T. ) ;
#5309=ORIENTED_EDGE ( 'NONE', *, *, #1479, .F. ) ;
#5315=AXIS2_PLACEMENT_3D ( 'NONE', #684, #1181, #3760 ) ;
#5336=LINE ( 'NONE', #7893, #3619 ) ;
#5348=ORIENTED_EDGE ( 'NONE', *, *, #7148, .F. ) ;
#5357=CARTESIAN_POINT ( 'NONE',  ( 2.750000000000000444, 7.964000000000000412, 3.833750000000001545 ) ) ;
#5360=DIRECTION ( 'NONE',  ( 1.000000000000000000, 0.000000000000000000, 0.000000000000000000 ) ) ;
#5362=VERTEX_POINT ( 'NONE', #183 ) ;
#5376=CARTESIAN_POINT ( 'NONE',  ( -2.750000000000000444, 8.729000000000002757, 3.833750000000001545 ) ) ;
#5390=CARTESIAN_POINT ( 'NONE',  ( -2.740000000000001545, 7.964000000000000412, 4.313750000000002416 ) ) ;
#5392=CARTESIAN_POINT ( 'NONE',  ( -2.740000000000001545, 7.964000000000000412, 3.833750000000001545 ) ) ;
#5399=DIRECTION ( 'NONE',  ( -0.7071067811865474617, -0.000000000000000000, 0.7071067811865474617 ) ) ;
#5406=VECTOR ( 'NONE', #4266, 39.37007874015748143 ) ;
#5419=( GEOMETRIC_REPRESENTATION_CONTEXT ( 3 ) GLOBAL_UNCERTAINTY_ASSIGNED_CONTEXT ( ( #955 ) ) GLOBAL_UNIT_ASSIGNED_CONTEXT ( ( #2427, #1765, #1688 ) ) REPRESENTATION_CONTEXT ( 'NONE', 'WORKASPACE' ) );
#5423=CARTESIAN_POINT ( 'NONE',  ( 2.745000000000000995, 8.719000000000002970, 3.828750000000002096 ) ) ;
#5429=VERTEX_POINT ( 'NONE', #1587 ) ;
#5446=VECTOR ( 'NONE', #3541, 39.37007874015748143 ) ;
#5451=AXIS2_PLACEMENT_3D ( 'NONE', #5392, #4078, #1722 ) ;
#5466=DIRECTION ( 'NONE',  ( 0.7071067811865475727, -0.7071067811865475727, 0.000000000000000000 ) ) ;
#5487=VERTEX_POINT ( 'NONE', #1707 ) ;
#5517=PLANE ( 'NONE',  #3047 ) ;
#5520=FACE_OUTER_BOUND ( 'NONE', #5012, .T. ) ;
#5537=ADVANCED_FACE ( 'NONE', ( #6704 ), #6006, .T. ) ;
#5555=ORIENTED_EDGE ( 'NONE', *, *, #4439, .T. ) ;
#5568=ORIENTED_EDGE ( 'NONE', *, *, #6187, .T. ) ;
#5585=VECTOR ( 'NONE', #7605, 39.37007874015748143 ) ;
#5618=DIRECTION ( 'NONE',  ( 1.000000000000000000, 0.000000000000000000, 0.000000000000000000 ) ) ;
#5651=APPLICATION_CONTEXT ( 'configuration controlled 3d designs of mechanical parts and assemblies' ) ;
#5654=ORIENTED_EDGE ( 'NONE', *, *, #4388, .T. ) ;
#5661=DIRECTION ( 'NONE',  ( 0.7071067811865475727, 0.000000000000000000, -0.7071067811865475727 ) ) ;
#5676=ORIENTED_EDGE ( 'NONE', *, *, #2551, .F. ) ;
#5681=DIRECTION ( 'NONE',  ( 0.000000000000000000, 0.000000000000000000, -1.000000000000000000 ) ) ;
#5682=VECTOR ( 'NONE', #6255, 39.37007874015748854 ) ;
#5688=VERTEX_POINT ( 'NONE', #1445 ) ;
#5700=LINE ( 'NONE', #5744, #579 ) ;
#5707=VECTOR ( 'NONE', #4296, 39.37007874015748854 ) ;
#5736=DIRECTION ( 'NONE',  ( -0.7071067811865474617, 0.7071067811865474617, -0.000000000000000000 ) ) ;
#5743=ADVANCED_FACE ( 'NONE', ( #6363 ), #5747, .T. ) ;
#5744=CARTESIAN_POINT ( 'NONE',  ( -2.740000000000001545, 7.964000000000000412, 3.823750000000002647 ) ) ;
#5745=PRODUCT ( 'bench vise5-', 'bench vise5-', '', ( #1171 ) ) ;
#5747=PLANE ( 'NONE',  #7268 ) ;
#5758=EDGE_LOOP ( 'NONE', ( #4633, #528, #5110, #550 ) ) ;
#5765=DIRECTION ( 'NONE',  ( 0.000000000000000000, -1.000000000000000000, 0.000000000000000000 ) ) ;
#5766=LINE ( 'NONE', #6917, #1355 ) ;
#5768=ORIENTED_EDGE ( 'NONE', *, *, #1683, .T. ) ;
#5770=LINE ( 'NONE', #689, #742 ) ;
#5778=ADVANCED_FACE ( 'NONE', ( #865 ), #3364, .T. ) ;
#5787=ADVANCED_FACE ( 'NONE', ( #7785 ), #373, .F. ) ;
#5838=DIRECTION ( 'NONE',  ( 0.000000000000000000, 0.000000000000000000, -1.000000000000000000 ) ) ;
#5859=DIRECTION ( 'NONE',  ( 0.000000000000000000, 0.000000000000000000, 1.000000000000000000 ) ) ;
#5871=CARTESIAN_POINT ( 'NONE',  ( 2.750000000000000444, 7.964000000000000412, 3.823750000000002647 ) ) ;
#5872=ORIENTED_EDGE ( 'NONE', *, *, #1683, .F. ) ;
#5883=DIRECTION ( 'NONE',  ( 0.000000000000000000, 1.000000000000000000, 0.000000000000000000 ) ) ;
#5901=EDGE_CURVE ( 'NONE', #5688, #4355, #2904, .T. ) ;
#5909=DIRECTION ( 'NONE',  ( 0.000000000000000000, -0.7071067811865474617, 0.7071067811865474617 ) ) ;
#5939=ADVANCED_FACE ( 'NONE', ( #5520 ), #3072, .T. ) ;
#5953=LINE ( 'NONE', #336, #574 ) ;
#5994=VECTOR ( 'NONE', #5736, 39.37007874015748854 ) ;
#6006=PLANE ( 'NONE',  #7815 ) ;
#6016=EDGE_LOOP ( 'NONE', ( #7799, #2843, #3293 ) ) ;
#6051=ORIENTED_EDGE ( 'NONE', *, *, #1778, .T. ) ;
#6069=ORIENTED_EDGE ( 'NONE', *, *, #1876, .T. ) ;
#6087=LINE ( 'NONE', #472, #1354 ) ;
#6089=EDGE_LOOP ( 'NONE', ( #998, #4479, #7252, #6738 ) ) ;
#6097=CARTESIAN_POINT ( 'NONE',  ( -2.740000000000001545, 7.964000000000000412, 4.313750000000002416 ) ) ;
#6099=CARTESIAN_POINT ( 'NONE',  ( -2.740000000000001545, 8.719000000000002970, 3.823750000000002647 ) ) ;
#6101=VECTOR ( 'NONE', #831, 39.37007874015748854 ) ;
#6140=ORIENTED_EDGE ( 'NONE', *, *, #4183, .F. ) ;
#6146=FACE_OUTER_BOUND ( 'NONE', #146, .T. ) ;
#6179=DIRECTION ( 'NONE',  ( 1.000000000000000000, 0.000000000000000000, -0.000000000000000000 ) ) ;
#6185=ORIENTED_EDGE ( 'NONE', *, *, #2568, .T. ) ;
#6187=EDGE_CURVE ( 'NONE', #4355, #5130, #5193, .T. ) ;
#6237=DIRECTION ( 'NONE',  ( 0.000000000000000000, 0.000000000000000000, 1.000000000000000000 ) ) ;
#6255=DIRECTION ( 'NONE',  ( -0.7071067811865474617, 0.000000000000000000, 0.7071067811865474617 ) ) ;
#6279=ORIENTED_EDGE ( 'NONE', *, *, #6709, .F. ) ;
#6296=CARTESIAN_POINT ( 'NONE',  ( -2.740000000000001545, 7.964000000000000412, 4.313750000000002416 ) ) ;
#6304=FACE_OUTER_BOUND ( 'NONE', #3156, .T. ) ;
#6315=FACE_OUTER_BOUND ( 'NONE', #7169, .T. ) ;
#6328=ORIENTED_EDGE ( 'NONE', *, *, #1327, .F. ) ;
#6329=LINE ( 'NONE', #3817, #1916 ) ;
#6334=ADVANCED_FACE ( 'NONE', ( #2126 ), #2742, .T. ) ;
#6363=FACE_OUTER_BOUND ( 'NONE', #31, .T. ) ;
#6377=VECTOR ( 'NONE', #7014, 39.37007874015748143 ) ;
#6405=EDGE_CURVE ( 'NONE', #2476, #2954, #2287, .T. ) ;
#6416=CARTESIAN_POINT ( 'NONE',  ( -2.750000000000000444, 8.719000000000002970, 4.313750000000002416 ) ) ;
#6421=PLANE ( 'NONE',  #2437 ) ;
#6437=CARTESIAN_POINT ( 'NONE',  ( 2.750000000000000444, 7.973999999999999311, 3.833750000000001545 ) ) ;
#6455=CARTESIAN_POINT ( 'NONE',  ( -2.740000000000001545, 8.729000000000002757, 3.833750000000001545 ) ) ;
#6471=CARTESIAN_POINT ( 'NONE',  ( 2.750000000000000444, 7.964000000000000412, 4.313750000000002416 ) ) ;
#6475=VECTOR ( 'NONE', #6891, 39.37007874015748854 ) ;
#6476=ORIENTED_EDGE ( 'NONE', *, *, #2882, .F. ) ;
#6483=EDGE_LOOP ( 'NONE', ( #3495, #1384, #577, #3403 ) ) ;
#6484=AXIS2_PLACEMENT_3D ( 'NONE', #1608, #995, #3491 ) ;
#6551=EDGE_CURVE ( 'NONE', #5487, #3887, #4291, .T. ) ;
#6557=CARTESIAN_POINT ( 'NONE',  ( 0.000000000000000000, 8.719000000000002970, 4.323750000000001315 ) ) ;
#6579=ADVANCED_FACE ( 'NONE', ( #1425 ), #6421, .T. ) ;
#6581=DIRECTION ( 'NONE',  ( 0.000000000000000000, -0.7071067811865475727, -0.7071067811865475727 ) ) ;
#6624=LINE ( 'NONE', #7275, #6899 ) ;
#6635=VERTEX_POINT ( 'NONE', #6951 ) ;
#6643=DIRECTION ( 'NONE',  ( 0.000000000000000000, 0.000000000000000000, -1.000000000000000000 ) ) ;
#6644=ORIENTED_EDGE ( 'NONE', *, *, #501, .F. ) ;
#6654=AXIS2_PLACEMENT_3D ( 'NONE', #3026, #4386, #697 ) ;
#6661=DIRECTION ( 'NONE',  ( 0.000000000000000000, 0.000000000000000000, -1.000000000000000000 ) ) ;
#6671=ORIENTED_EDGE ( 'NONE', *, *, #6405, .F. ) ;
#6673=PLANE ( 'NONE',  #3214 ) ;
#6704=FACE_OUTER_BOUND ( 'NONE', #101, .T. ) ;
#6708=CARTESIAN_POINT ( 'NONE',  ( -2.740000000000001545, 8.729000000000002757, 4.313750000000002416 ) ) ;
#6709=EDGE_CURVE ( 'NONE', #2620, #3365, #4367, .T. ) ;
#6723=( LENGTH_UNIT ( ) NAMED_UNIT ( * ) SI_UNIT ( $, .METRE. ) );
#6729=LINE ( 'NONE', #1118, #7319 ) ;
#6738=ORIENTED_EDGE ( 'NONE', *, *, #2346, .F. ) ;
#6741=CARTESIAN_POINT ( 'NONE',  ( -2.745000000000000995, 7.973999999999999311, 4.318750000000002309 ) ) ;
#6751=VECTOR ( 'NONE', #4531, 39.37007874015748854 ) ;
#6771=EDGE_LOOP ( 'NONE', ( #7680, #7623, #7585, #2915 ) ) ;
#6790=FACE_OUTER_BOUND ( 'NONE', #774, .T. ) ;
#6792=CARTESIAN_POINT ( 'NONE',  ( 2.750000000000000444, 8.719000000000002970, 4.313750000000002416 ) ) ;
#6796=DIRECTION ( 'NONE',  ( 0.000000000000000000, -1.000000000000000000, 0.000000000000000000 ) ) ;
#6798=LINE ( 'NONE', #1872, #75 ) ;
#6800=DIRECTION ( 'NONE',  ( -0.7071067811865475727, -0.7071067811865475727, 0.000000000000000000 ) ) ;
#6807=CARTESIAN_POINT ( 'NONE',  ( -2.750000000000000444, 7.964000000000000412, 4.313750000000002416 ) ) ;
#6812=LINE ( 'NONE', #8185, #6475 ) ;
#6821=ORIENTED_EDGE ( 'NONE', *, *, #3268, .T. ) ;
#6857=DIRECTION ( 'NONE',  ( 0.7071067811865474617, -0.000000000000000000, -0.7071067811865474617 ) ) ;
#6891=DIRECTION ( 'NONE',  ( -0.7071067811865474617, -0.7071067811865474617, -0.000000000000000000 ) ) ;
#6898=VECTOR ( 'NONE', #2656, 39.37007874015748143 ) ;
#6899=VECTOR ( 'NONE', #3568, 39.37007874015748143 ) ;
#6907=ORIENTED_EDGE ( 'NONE', *, *, #237, .T. ) ;
#6916=DIRECTION ( 'NONE',  ( -0.7071067811865474617, 0.7071067811865474617, -0.000000000000000000 ) ) ;
#6917=CARTESIAN_POINT ( 'NONE',  ( 2.740000000000001545, 8.729000000000002757, 3.823750000000002647 ) ) ;
#6930=FACE_OUTER_BOUND ( 'NONE', #2135, .T. ) ;
#6931=ADVANCED_FACE ( 'NONE', ( #1056 ), #6673, .F. ) ;
#6938=EDGE_CURVE ( 'NONE', #5487, #4455, #4816, .T. ) ;
#6947=DIRECTION ( 'NONE',  ( 0.000000000000000000, 0.7071067811865474617, 0.7071067811865474617 ) ) ;
#6951=CARTESIAN_POINT ( 'NONE',  ( -2.750000000000000444, 7.973999999999999311, 4.313750000000002416 ) ) ;
#6967=LINE ( 'NONE', #7535, #6377 ) ;
#7000=VECTOR ( 'NONE', #93, 39.37007874015748854 ) ;
#7014=DIRECTION ( 'NONE',  ( 1.000000000000000000, 0.000000000000000000, 0.000000000000000000 ) ) ;
#7016=AXIS2_PLACEMENT_3D ( 'NONE', #5376, #3509, #7932 ) ;
#7017=DIMENSIONAL_EXPONENTS ( 1.000000000000000000, 0.000000000000000000, 0.000000000000000000, 0.000000000000000000, 0.000000000000000000, 0.000000000000000000, 0.000000000000000000 ) ;
#7066=ORIENTED_EDGE ( 'NONE', *, *, #7755, .F. ) ;
#7092=DIRECTION ( 'NONE',  ( 0.5773502691896257311, -0.5773502691896257311, -0.5773502691896257311 ) ) ;
#7113=VERTEX_POINT ( 'NONE', #3746 ) ;
#7116=VECTOR ( 'NONE', #1130, 39.37007874015748854 ) ;
#7148=EDGE_CURVE ( 'NONE', #5130, #2954, #6329, .T. ) ;
#7169=EDGE_LOOP ( 'NONE', ( #7632, #3355, #2120, #6328 ) ) ;
#7185=CARTESIAN_POINT ( 'NONE',  ( 2.750000000000000444, 8.729000000000002757, 4.313750000000002416 ) ) ;
#7199=EDGE_CURVE ( 'NONE', #5688, #1328, #2228, .T. ) ;
#7219=ADVANCED_BREP_SHAPE_REPRESENTATION ( '', ( #1772, #7272 ), #5419 ) ;
#7252=ORIENTED_EDGE ( 'NONE', *, *, #3268, .F. ) ;
#7262=VERTEX_POINT ( 'NONE', #2760 ) ;
#7268=AXIS2_PLACEMENT_3D ( 'NONE', #5160, #7706, #704 ) ;
#7272=AXIS2_PLACEMENT_3D ( 'NONE', #3736, #6237, #5618 ) ;
#7275=CARTESIAN_POINT ( 'NONE',  ( 2.750000000000000444, 8.719000000000002970, 3.823750000000002647 ) ) ;
#7304=DIRECTION ( 'NONE',  ( -0.000000000000000000, 0.7071067811865474617, -0.7071067811865474617 ) ) ;
#7319=VECTOR ( 'NONE', #500, 39.37007874015748143 ) ;
#7321=CARTESIAN_POINT ( 'NONE',  ( -2.740000000000001545, 8.724000000000001975, 3.828750000000002096 ) ) ;
#7335=DIRECTION ( 'NONE',  ( 0.000000000000000000, -1.000000000000000000, 0.000000000000000000 ) ) ;
#7353=DIRECTION ( 'NONE',  ( 1.000000000000000000, 0.000000000000000000, -0.000000000000000000 ) ) ;
#7376=LINE ( 'NONE', #6741, #7808 ) ;
#7395=VECTOR ( 'NONE', #5838, 39.37007874015748143 ) ;
#7411=AXIS2_PLACEMENT_3D ( 'NONE', #3398, #7867, #6643 ) ;
#7427=CLOSED_SHELL ( 'NONE', ( #411, #5778, #686, #4285, #5939, #3346, #6931, #5537, #5743, #345, #5787, #1748, #1502, #327, #4940, #2129, #6579, #6334, #2387, #1447, #3983, #8158, #4721, #2441, #1674, #4025 ) ) ;
#7463=PLANE ( 'NONE',  #3459 ) ;
#7466=ORIENTED_EDGE ( 'NONE', *, *, #6405, .T. ) ;
#7503=CARTESIAN_POINT ( 'NONE',  ( -2.750000000000000444, 8.719000000000002970, 3.823750000000002647 ) ) ;
#7535=CARTESIAN_POINT ( 'NONE',  ( 2.750000000000000444, 8.729000000000002757, 4.313750000000002416 ) ) ;
#7537=VECTOR ( 'NONE', #4666, 39.37007874015748854 ) ;
#7540=VECTOR ( 'NONE', #6857, 39.37007874015748854 ) ;
#7584=DIRECTION ( 'NONE',  ( 0.7071067811865475727, 0.000000000000000000, -0.7071067811865475727 ) ) ;
#7585=ORIENTED_EDGE ( 'NONE', *, *, #2443, .T. ) ;
#7605=DIRECTION ( 'NONE',  ( 0.000000000000000000, -1.000000000000000000, 0.000000000000000000 ) ) ;
#7623=ORIENTED_EDGE ( 'NONE', *, *, #5301, .T. ) ;
#7625=DESIGN_CONTEXT ( 'detailed design', #1532, 'design' ) ;
#7632=ORIENTED_EDGE ( 'NONE', *, *, #3431, .T. ) ;
#7670=EDGE_CURVE ( 'NONE', #5362, #941, #2968, .T. ) ;
#7680=ORIENTED_EDGE ( 'NONE', *, *, #8012, .T. ) ;
#7705=CARTESIAN_POINT ( 'NONE',  ( 2.740000000000001545, 7.964000000000000412, 3.823750000000002647 ) ) ;
#7706=DIRECTION ( 'NONE',  ( -0.5773502691896257311, 0.5773502691896257311, -0.5773502691896257311 ) ) ;
#7734=ORIENTED_EDGE ( 'NONE', *, *, #7755, .T. ) ;
#7740=LINE ( 'NONE', #8084, #5707 ) ;
#7742=ORIENTED_EDGE ( 'NONE', *, *, #4131, .F. ) ;
#7755=EDGE_CURVE ( 'NONE', #7113, #212, #2820, .T. ) ;
#7781=EDGE_CURVE ( 'NONE', #520, #4455, #6087, .T. ) ;
#7785=FACE_OUTER_BOUND ( 'NONE', #3740, .T. ) ;
#7799=ORIENTED_EDGE ( 'NONE', *, *, #2493, .T. ) ;
#7805=DIRECTION ( 'NONE',  ( -1.000000000000000000, 0.000000000000000000, 0.000000000000000000 ) ) ;
#7808=VECTOR ( 'NONE', #1244, 39.37007874015748854 ) ;
#7814=CARTESIAN_POINT ( 'NONE',  ( -2.750000000000000444, 7.973999999999999311, 3.833750000000001545 ) ) ;
#7815=AXIS2_PLACEMENT_3D ( 'NONE', #3543, #2885, #4279 ) ;
#7817=VERTEX_POINT ( 'NONE', #6455 ) ;
#7821=ORIENTED_EDGE ( 'NONE', *, *, #3739, .T. ) ;
#7841=CARTESIAN_POINT ( 'NONE',  ( 2.750000000000000444, 7.964000000000000412, 4.313750000000002416 ) ) ;
#7865=CARTESIAN_POINT ( 'NONE',  ( -2.745000000000000995, 8.719000000000002970, 4.318750000000002309 ) ) ;
#7867=DIRECTION ( 'NONE',  ( 0.7071067811865475727, 0.7071067811865475727, 0.000000000000000000 ) ) ;
#7885=EDGE_CURVE ( 'NONE', #3887, #1328, #5287, .T. ) ;
#7893=CARTESIAN_POINT ( 'NONE',  ( 2.750000000000000444, 8.729000000000002757, 3.833750000000001545 ) ) ;
#7906=ORIENTED_EDGE ( 'NONE', *, *, #7781, .F. ) ;
#7911=ORIENTED_EDGE ( 'NONE', *, *, #2928, .T. ) ;
#7932=DIRECTION ( 'NONE',  ( 0.000000000000000000, 1.000000000000000000, 0.000000000000000000 ) ) ;
#7933=EDGE_LOOP ( 'NONE', ( #248, #5555, #1985, #5654 ) ) ;
#7935=DIRECTION ( 'NONE',  ( 0.000000000000000000, 0.000000000000000000, -1.000000000000000000 ) ) ;
#7948=DIRECTION ( 'NONE',  ( 0.000000000000000000, -0.7071067811865474617, -0.7071067811865474617 ) ) ;
#7954=VECTOR ( 'NONE', #5909, 39.37007874015748854 ) ;
#7958=LENGTH_MEASURE_WITH_UNIT ( LENGTH_MEASURE( 0.02539999999999999897 ), #6723 );
#8012=EDGE_CURVE ( 'NONE', #4355, #1456, #1196, .T. ) ;
#8031=CARTESIAN_POINT ( 'NONE',  ( 2.740000000000001545, 7.964000000000000412, 4.313750000000002416 ) ) ;
#8033=ORIENTED_EDGE ( 'NONE', *, *, #731, .F. ) ;
#8084=CARTESIAN_POINT ( 'NONE',  ( 2.740000000000001545, 8.724000000000001975, 4.318750000000002309 ) ) ;
#8105=ORIENTED_EDGE ( 'NONE', *, *, #6551, .F. ) ;
#8158=ADVANCED_FACE ( 'NONE', ( #703 ), #3160, .T. ) ;
#8172=LINE ( 'NONE', #4373, #3219 ) ;
#8176=EDGE_CURVE ( 'NONE', #7262, #1328, #1934, .T. ) ;
#8185=CARTESIAN_POINT ( 'NONE',  ( -2.740000000000001545, 8.729000000000002757, 4.313750000000002416 ) ) ;
#8199=COLOUR_RGB('Deep Blue', 0.66274510, 0.83137255, 0.94901961);
#8200=FILL_AREA_STYLE_COLOUR('',#8199);
#8201=FILL_AREA_STYLE('',(#8200));
#8202=SURFACE_STYLE_FILL_AREA(#8201);
#8203=SURFACE_SIDE_STYLE('',(#8202));
#8204=SURFACE_STYLE_USAGE(.BOTH.,#8203);
#8205=PRESENTATION_STYLE_ASSIGNMENT((#8204));
#8259=STYLED_ITEM('',(#8205),#1772);
#8260=MECHANICAL_DESIGN_GEOMETRIC_PRESENTATION_REPRESENTATION('',(#8259),#5419);
ENDSEC;
END-ISO-10303-21;
